ISO-10303-21;
HEADER;
/* Generated by software containing ST-Developer
 * from STEP Tools, Inc. (www.steptools.com) 
 */

FILE_DESCRIPTION(
/* description */ ('Flywheel Crank-Slider'),
/* implementation_level */ '2;1');

FILE_NAME(
/* name */ 'Rod bearing retainer (2).step',
/* time_stamp */ '2026-10-28T03:23:13-07:00',
/* author */ (''),
/* organization */ (''),
/* preprocessor_version */ 'ST-DEVELOPER v20.2',
/* originating_system */ 'Autodesk Translation Framework v15.17.0.0',
/* authorisation */ '');

FILE_SCHEMA (('AUTOMOTIVE_DESIGN { 1 0 10303 214 3 1 1 }'));
ENDSEC;

DATA;
#10=MECHANICAL_DESIGN_GEOMETRIC_PRESENTATION_REPRESENTATION('',(#704),#17322);
#599=SHAPE_REPRESENTATION_RELATIONSHIP('SRR','None',#17598,#651);
#651=ADVANCED_BREP_SHAPE_REPRESENTATION('',(#761),#17302);
#704=STYLED_ITEM('',(#17931),#761);
#761=MANIFOLD_SOLID_BREP('Body1',#9086);
#939=FACE_BOUND('',#2386,.T.);
#940=FACE_BOUND('',#2388,.T.);
#1238=PLANE('',#10382);
#1239=PLANE('',#10383);
#1694=FACE_OUTER_BOUND('',#2383,.T.);
#1695=FACE_OUTER_BOUND('',#2384,.T.);
#1696=FACE_OUTER_BOUND('',#2385,.T.);
#1697=FACE_OUTER_BOUND('',#2387,.T.);
#2383=EDGE_LOOP('',(#7674,#7675,#7676,#7677));
#2384=EDGE_LOOP('',(#7678,#7679,#7680,#7681));
#2385=EDGE_LOOP('',(#7682));
#2386=EDGE_LOOP('',(#7683));
#2387=EDGE_LOOP('',(#7684));
#2388=EDGE_LOOP('',(#7685));
#3082=LINE('',#16023,#3693);
#3083=LINE('',#16029,#3694);
#3693=VECTOR('',#12682,1.1);
#3694=VECTOR('',#12689,2.);
#4112=CIRCLE('',#10377,1.1);
#4113=CIRCLE('',#10378,1.1);
#4114=CIRCLE('',#10380,2.);
#4115=CIRCLE('',#10381,2.);
#4791=VERTEX_POINT('',#16020);
#4792=VERTEX_POINT('',#16022);
#4793=VERTEX_POINT('',#16026);
#4794=VERTEX_POINT('',#16028);
#5794=EDGE_CURVE('',#4791,#4791,#4112,.T.);
#5795=EDGE_CURVE('',#4791,#4792,#3082,.T.);
#5796=EDGE_CURVE('',#4792,#4792,#4113,.T.);
#5797=EDGE_CURVE('',#4793,#4793,#4114,.T.);
#5798=EDGE_CURVE('',#4793,#4794,#3083,.T.);
#5799=EDGE_CURVE('',#4794,#4794,#4115,.T.);
#7674=ORIENTED_EDGE('',*,*,#5794,.F.);
#7675=ORIENTED_EDGE('',*,*,#5795,.T.);
#7676=ORIENTED_EDGE('',*,*,#5796,.T.);
#7677=ORIENTED_EDGE('',*,*,#5795,.F.);
#7678=ORIENTED_EDGE('',*,*,#5797,.F.);
#7679=ORIENTED_EDGE('',*,*,#5798,.T.);
#7680=ORIENTED_EDGE('',*,*,#5799,.T.);
#7681=ORIENTED_EDGE('',*,*,#5798,.F.);
#7682=ORIENTED_EDGE('',*,*,#5797,.T.);
#7683=ORIENTED_EDGE('',*,*,#5794,.T.);
#7684=ORIENTED_EDGE('',*,*,#5799,.F.);
#7685=ORIENTED_EDGE('',*,*,#5796,.F.);
#8457=CYLINDRICAL_SURFACE('',#10376,1.1);
#8458=CYLINDRICAL_SURFACE('',#10379,2.);
#8885=ADVANCED_FACE('',(#1694),#8457,.F.);
#8886=ADVANCED_FACE('',(#1695),#8458,.T.);
#8887=ADVANCED_FACE('',(#1696,#939),#1238,.T.);
#8888=ADVANCED_FACE('',(#1697,#940),#1239,.F.);
#9086=CLOSED_SHELL('',(#8885,#8886,#8887,#8888));
#10375=AXIS2_PLACEMENT_3D('',#16018,#12676,#12677);
#10376=AXIS2_PLACEMENT_3D('',#16019,#12678,#12679);
#10377=AXIS2_PLACEMENT_3D('',#16021,#12680,#12681);
#10378=AXIS2_PLACEMENT_3D('',#16024,#12683,#12684);
#10379=AXIS2_PLACEMENT_3D('',#16025,#12685,#12686);
#10380=AXIS2_PLACEMENT_3D('',#16027,#12687,#12688);
#10381=AXIS2_PLACEMENT_3D('',#16030,#12690,#12691);
#10382=AXIS2_PLACEMENT_3D('',#16031,#12692,#12693);
#10383=AXIS2_PLACEMENT_3D('',#16032,#12694,#12695);
#12676=DIRECTION('axis',(0.,0.,1.));
#12677=DIRECTION('refdir',(1.,0.,0.));
#12678=DIRECTION('center_axis',(0.,1.,0.));
#12679=DIRECTION('ref_axis',(1.,0.,0.));
#12680=DIRECTION('center_axis',(0.,-1.,0.));
#12681=DIRECTION('ref_axis',(1.,0.,0.));
#12682=DIRECTION('',(0.,-1.,0.));
#12683=DIRECTION('center_axis',(0.,-1.,0.));
#12684=DIRECTION('ref_axis',(1.,0.,0.));
#12685=DIRECTION('center_axis',(0.,1.,0.));
#12686=DIRECTION('ref_axis',(1.,0.,0.));
#12687=DIRECTION('center_axis',(0.,1.,0.));
#12688=DIRECTION('ref_axis',(1.,0.,0.));
#12689=DIRECTION('',(0.,-1.,0.));
#12690=DIRECTION('center_axis',(0.,1.,0.));
#12691=DIRECTION('ref_axis',(1.,0.,0.));
#12692=DIRECTION('center_axis',(0.,1.,0.));
#12693=DIRECTION('ref_axis',(1.,0.,0.));
#12694=DIRECTION('center_axis',(0.,1.,0.));
#12695=DIRECTION('ref_axis',(1.,0.,0.));
#16018=CARTESIAN_POINT('',(0.,0.,0.));
#16019=CARTESIAN_POINT('Origin',(12.,2.3,10.));
#16020=CARTESIAN_POINT('',(10.9,2.5,10.));
#16021=CARTESIAN_POINT('Origin',(12.,2.5,10.));
#16022=CARTESIAN_POINT('',(10.9,2.3,10.));
#16023=CARTESIAN_POINT('',(10.9,2.3,10.));
#16024=CARTESIAN_POINT('Origin',(12.,2.3,10.));
#16025=CARTESIAN_POINT('Origin',(12.,2.3,10.));
#16026=CARTESIAN_POINT('',(10.,2.5,10.));
#16027=CARTESIAN_POINT('Origin',(12.,2.5,10.));
#16028=CARTESIAN_POINT('',(10.,2.3,10.));
#16029=CARTESIAN_POINT('',(10.,2.3,10.));
#16030=CARTESIAN_POINT('Origin',(12.,2.3,10.));
#16031=CARTESIAN_POINT('Origin',(12.,2.5,10.));
#16032=CARTESIAN_POINT('Origin',(12.,2.3,10.));
#17241=UNCERTAINTY_MEASURE_WITH_UNIT(LENGTH_MEASURE(0.001),#17323,
'DISTANCE_ACCURACY_VALUE',
'Maximum model space distance between geometric entities at asserted c
onnectivities');
#17261=UNCERTAINTY_MEASURE_WITH_UNIT(LENGTH_MEASURE(0.001),#17323,
'DISTANCE_ACCURACY_VALUE',
'Maximum model space distance between geometric entities at asserted c
onnectivities');
#17302=(
GEOMETRIC_REPRESENTATION_CONTEXT(3)
GLOBAL_UNCERTAINTY_ASSIGNED_CONTEXT((#17241))
GLOBAL_UNIT_ASSIGNED_CONTEXT((#17323,#17325,#17326))
REPRESENTATION_CONTEXT('','3D')
);
#17322=(
GEOMETRIC_REPRESENTATION_CONTEXT(3)
GLOBAL_UNCERTAINTY_ASSIGNED_CONTEXT((#17261))
GLOBAL_UNIT_ASSIGNED_CONTEXT((#17323,#17325,#17326))
REPRESENTATION_CONTEXT('','3D')
);
#17323=(
LENGTH_UNIT()
NAMED_UNIT(*)
SI_UNIT(.CENTI.,.METRE.)
);
#17325=(
NAMED_UNIT(*)
PLANE_ANGLE_UNIT()
SI_UNIT($,.RADIAN.)
);
#17326=(
NAMED_UNIT(*)
SI_UNIT($,.STERADIAN.)
SOLID_ANGLE_UNIT()
);
#17367=SHAPE_DEFINITION_REPRESENTATION(#17429,#17598);
#17429=PRODUCT_DEFINITION_SHAPE('',$,#17659);
#17598=SHAPE_REPRESENTATION('',(#10375),#17302);
#17618=PRODUCT_DEFINITION_CONTEXT('part definition',#17800,'design');
#17659=PRODUCT_DEFINITION('Rod bearing retainer (2)',
'Rod bearing retainer (2)',#17719,#17618);
#17719=PRODUCT_DEFINITION_FORMATION('',$,#17842);
#17800=APPLICATION_CONTEXT(
'Core Data for Automotive Mechanical Design Process');
#17801=PRODUCT_CONTEXT('part definition',#17800,'mechanical');
#17842=PRODUCT('Rod bearing retainer (2)','Rod bearing retainer (2)',
'Rod bearing retainer (2)',(#17801));
#17925=COLOUR_RGB('Grey',0.48,0.52,0.57);
#17926=FILL_AREA_STYLE_COLOUR('',#17925);
#17927=FILL_AREA_STYLE('',(#17926));
#17928=SURFACE_STYLE_FILL_AREA(#17927);
#17929=SURFACE_SIDE_STYLE('',(#17928));
#17930=SURFACE_STYLE_USAGE(.BOTH.,#17929);
#17931=PRESENTATION_STYLE_ASSIGNMENT((#17930));
ENDSEC;
END-ISO-10303-21;
